ISO-10303-21;
HEADER;
/* Generated by software containing ST-Developer
 * from STEP Tools, Inc. (www.steptools.com) 
 */

FILE_DESCRIPTION(
/* description */ ('Door-style hinge test fixture with detent'),
/* implementation_level */ '2;1');

FILE_NAME(
/* name */ 'Cap Screw - M4x16.step',
/* time_stamp */ '2026-10-28T03:24:57-07:00',
/* author */ (''),
/* organization */ (''),
/* preprocessor_version */ 'ST-DEVELOPER v20.2',
/* originating_system */ 'Autodesk Translation Framework v15.17.0.0',
/* authorisation */ '');

FILE_SCHEMA (('AUTOMOTIVE_DESIGN { 1 0 10303 214 3 1 1 }'));
ENDSEC;

DATA;
#10=MECHANICAL_DESIGN_GEOMETRIC_PRESENTATION_REPRESENTATION('',(#361),#9813);
#211=CONICAL_SURFACE('',#5719,0.325,0.785398163397448);
#212=CONICAL_SURFACE('',#5723,0.335,0.785398163397448);
#213=CONICAL_SURFACE('',#5727,0.21,0.463647609000806);
#214=CONICAL_SURFACE('',#5731,0.18,0.785398163397448);
#217=ORIENTED_CLOSED_SHELL('',*,#4795,.F.);
#220=BREP_WITH_VOIDS('Body1',#4794,(#217));
#290=SHAPE_REPRESENTATION_RELATIONSHIP('SRR','None',#9969,#321);
#321=ADVANCED_BREP_SHAPE_REPRESENTATION('',(#220),#9812);
#361=STYLED_ITEM('',(#10190),#220);
#499=FACE_BOUND('',#1321,.T.);
#652=PLANE('',#5717);
#653=PLANE('',#5725);
#654=PLANE('',#5733);
#655=PLANE('',#5734);
#656=PLANE('',#5735);
#657=PLANE('',#5736);
#658=PLANE('',#5737);
#659=PLANE('',#5738);
#660=PLANE('',#5739);
#661=PLANE('',#5740);
#662=PLANE('',#5741);
#931=FACE_OUTER_BOUND('',#1316,.T.);
#932=FACE_OUTER_BOUND('',#1317,.T.);
#933=FACE_OUTER_BOUND('',#1318,.T.);
#934=FACE_OUTER_BOUND('',#1319,.T.);
#935=FACE_OUTER_BOUND('',#1320,.T.);
#936=FACE_OUTER_BOUND('',#1322,.T.);
#937=FACE_OUTER_BOUND('',#1323,.T.);
#938=FACE_OUTER_BOUND('',#1324,.T.);
#939=FACE_OUTER_BOUND('',#1325,.T.);
#940=FACE_OUTER_BOUND('',#1326,.T.);
#941=FACE_OUTER_BOUND('',#1327,.T.);
#942=FACE_OUTER_BOUND('',#1328,.T.);
#943=FACE_OUTER_BOUND('',#1329,.T.);
#944=FACE_OUTER_BOUND('',#1330,.T.);
#945=FACE_OUTER_BOUND('',#1331,.T.);
#946=FACE_OUTER_BOUND('',#1332,.T.);
#947=FACE_OUTER_BOUND('',#1333,.T.);
#1316=EDGE_LOOP('',(#4317));
#1317=EDGE_LOOP('',(#4318,#4319,#4320,#4321));
#1318=EDGE_LOOP('',(#4322,#4323,#4324,#4325));
#1319=EDGE_LOOP('',(#4326,#4327,#4328,#4329));
#1320=EDGE_LOOP('',(#4330));
#1321=EDGE_LOOP('',(#4331));
#1322=EDGE_LOOP('',(#4332,#4333,#4334,#4335));
#1323=EDGE_LOOP('',(#4336,#4337,#4338,#4339));
#1324=EDGE_LOOP('',(#4340,#4341,#4342,#4343));
#1325=EDGE_LOOP('',(#4344));
#1326=EDGE_LOOP('',(#4345,#4346,#4347,#4348));
#1327=EDGE_LOOP('',(#4349,#4350,#4351,#4352));
#1328=EDGE_LOOP('',(#4353,#4354,#4355,#4356));
#1329=EDGE_LOOP('',(#4357,#4358,#4359,#4360));
#1330=EDGE_LOOP('',(#4361,#4362,#4363,#4364));
#1331=EDGE_LOOP('',(#4365,#4366,#4367,#4368));
#1332=EDGE_LOOP('',(#4369,#4370,#4371,#4372,#4373,#4374));
#1333=EDGE_LOOP('',(#4375,#4376,#4377,#4378,#4379,#4380));
#1630=LINE('',#9670,#1950);
#1631=LINE('',#9674,#1951);
#1632=LINE('',#9678,#1952);
#1633=LINE('',#9685,#1953);
#1634=LINE('',#9689,#1954);
#1635=LINE('',#9693,#1955);
#1636=LINE('',#9698,#1956);
#1637=LINE('',#9700,#1957);
#1638=LINE('',#9702,#1958);
#1639=LINE('',#9703,#1959);
#1640=LINE('',#9706,#1960);
#1641=LINE('',#9708,#1961);
#1642=LINE('',#9709,#1962);
#1643=LINE('',#9712,#1963);
#1644=LINE('',#9714,#1964);
#1645=LINE('',#9715,#1965);
#1646=LINE('',#9718,#1966);
#1647=LINE('',#9720,#1967);
#1648=LINE('',#9721,#1968);
#1649=LINE('',#9724,#1969);
#1650=LINE('',#9726,#1970);
#1651=LINE('',#9727,#1971);
#1652=LINE('',#9729,#1972);
#1653=LINE('',#9730,#1973);
#1950=VECTOR('',#7213,0.325);
#1951=VECTOR('',#7218,0.35);
#1952=VECTOR('',#7223,0.335);
#1953=VECTOR('',#7232,0.21);
#1954=VECTOR('',#7237,0.2);
#1955=VECTOR('',#7242,0.18);
#1956=VECTOR('',#7247,1.);
#1957=VECTOR('',#7248,1.);
#1958=VECTOR('',#7249,1.);
#1959=VECTOR('',#7250,1.);
#1960=VECTOR('',#7253,1.);
#1961=VECTOR('',#7254,1.);
#1962=VECTOR('',#7255,1.);
#1963=VECTOR('',#7258,1.);
#1964=VECTOR('',#7259,1.);
#1965=VECTOR('',#7260,1.);
#1966=VECTOR('',#7263,1.);
#1967=VECTOR('',#7264,1.);
#1968=VECTOR('',#7265,1.);
#1969=VECTOR('',#7268,1.);
#1970=VECTOR('',#7269,1.);
#1971=VECTOR('',#7270,1.);
#1972=VECTOR('',#7273,1.);
#1973=VECTOR('',#7274,1.);
#2213=CIRCLE('',#5718,0.3);
#2214=CIRCLE('',#5720,0.35);
#2215=CIRCLE('',#5722,0.35);
#2216=CIRCLE('',#5724,0.32);
#2217=CIRCLE('',#5726,0.22);
#2218=CIRCLE('',#5728,0.1954);
#2219=CIRCLE('',#5730,0.1954);
#2220=CIRCLE('',#5732,0.16);
#2600=VERTEX_POINT('',#9665);
#2601=VERTEX_POINT('',#9668);
#2602=VERTEX_POINT('',#9672);
#2603=VERTEX_POINT('',#9676);
#2604=VERTEX_POINT('',#9680);
#2605=VERTEX_POINT('',#9683);
#2606=VERTEX_POINT('',#9687);
#2607=VERTEX_POINT('',#9691);
#2608=VERTEX_POINT('',#9696);
#2609=VERTEX_POINT('',#9697);
#2610=VERTEX_POINT('',#9699);
#2611=VERTEX_POINT('',#9701);
#2612=VERTEX_POINT('',#9705);
#2613=VERTEX_POINT('',#9707);
#2614=VERTEX_POINT('',#9711);
#2615=VERTEX_POINT('',#9713);
#2616=VERTEX_POINT('',#9717);
#2617=VERTEX_POINT('',#9719);
#2618=VERTEX_POINT('',#9723);
#2619=VERTEX_POINT('',#9725);
#3175=EDGE_CURVE('',#2600,#2600,#2213,.T.);
#3176=EDGE_CURVE('',#2601,#2601,#2214,.T.);
#3177=EDGE_CURVE('',#2601,#2600,#1630,.T.);
#3178=EDGE_CURVE('',#2602,#2602,#2215,.T.);
#3179=EDGE_CURVE('',#2602,#2601,#1631,.T.);
#3180=EDGE_CURVE('',#2603,#2603,#2216,.T.);
#3181=EDGE_CURVE('',#2603,#2602,#1632,.T.);
#3182=EDGE_CURVE('',#2604,#2604,#2217,.T.);
#3183=EDGE_CURVE('',#2605,#2605,#2218,.F.);
#3184=EDGE_CURVE('',#2605,#2604,#1633,.T.);
#3185=EDGE_CURVE('',#2606,#2606,#2219,.F.);
#3186=EDGE_CURVE('',#2606,#2605,#1634,.T.);
#3187=EDGE_CURVE('',#2607,#2607,#2220,.T.);
#3188=EDGE_CURVE('',#2607,#2606,#1635,.T.);
#3189=EDGE_CURVE('',#2608,#2609,#1636,.T.);
#3190=EDGE_CURVE('',#2609,#2610,#1637,.T.);
#3191=EDGE_CURVE('',#2610,#2611,#1638,.T.);
#3192=EDGE_CURVE('',#2608,#2611,#1639,.T.);
#3193=EDGE_CURVE('',#2609,#2612,#1640,.T.);
#3194=EDGE_CURVE('',#2612,#2613,#1641,.T.);
#3195=EDGE_CURVE('',#2613,#2610,#1642,.T.);
#3196=EDGE_CURVE('',#2612,#2614,#1643,.T.);
#3197=EDGE_CURVE('',#2614,#2615,#1644,.T.);
#3198=EDGE_CURVE('',#2615,#2613,#1645,.T.);
#3199=EDGE_CURVE('',#2614,#2616,#1646,.T.);
#3200=EDGE_CURVE('',#2616,#2617,#1647,.T.);
#3201=EDGE_CURVE('',#2617,#2615,#1648,.T.);
#3202=EDGE_CURVE('',#2616,#2618,#1649,.T.);
#3203=EDGE_CURVE('',#2618,#2619,#1650,.T.);
#3204=EDGE_CURVE('',#2619,#2617,#1651,.T.);
#3205=EDGE_CURVE('',#2618,#2608,#1652,.T.);
#3206=EDGE_CURVE('',#2611,#2619,#1653,.T.);
#4317=ORIENTED_EDGE('',*,*,#3175,.F.);
#4318=ORIENTED_EDGE('',*,*,#3176,.F.);
#4319=ORIENTED_EDGE('',*,*,#3177,.T.);
#4320=ORIENTED_EDGE('',*,*,#3175,.T.);
#4321=ORIENTED_EDGE('',*,*,#3177,.F.);
#4322=ORIENTED_EDGE('',*,*,#3178,.F.);
#4323=ORIENTED_EDGE('',*,*,#3179,.T.);
#4324=ORIENTED_EDGE('',*,*,#3176,.T.);
#4325=ORIENTED_EDGE('',*,*,#3179,.F.);
#4326=ORIENTED_EDGE('',*,*,#3180,.F.);
#4327=ORIENTED_EDGE('',*,*,#3181,.T.);
#4328=ORIENTED_EDGE('',*,*,#3178,.T.);
#4329=ORIENTED_EDGE('',*,*,#3181,.F.);
#4330=ORIENTED_EDGE('',*,*,#3180,.T.);
#4331=ORIENTED_EDGE('',*,*,#3182,.F.);
#4332=ORIENTED_EDGE('',*,*,#3183,.F.);
#4333=ORIENTED_EDGE('',*,*,#3184,.T.);
#4334=ORIENTED_EDGE('',*,*,#3182,.T.);
#4335=ORIENTED_EDGE('',*,*,#3184,.F.);
#4336=ORIENTED_EDGE('',*,*,#3185,.F.);
#4337=ORIENTED_EDGE('',*,*,#3186,.T.);
#4338=ORIENTED_EDGE('',*,*,#3183,.T.);
#4339=ORIENTED_EDGE('',*,*,#3186,.F.);
#4340=ORIENTED_EDGE('',*,*,#3187,.F.);
#4341=ORIENTED_EDGE('',*,*,#3188,.T.);
#4342=ORIENTED_EDGE('',*,*,#3185,.T.);
#4343=ORIENTED_EDGE('',*,*,#3188,.F.);
#4344=ORIENTED_EDGE('',*,*,#3187,.T.);
#4345=ORIENTED_EDGE('',*,*,#3189,.T.);
#4346=ORIENTED_EDGE('',*,*,#3190,.T.);
#4347=ORIENTED_EDGE('',*,*,#3191,.T.);
#4348=ORIENTED_EDGE('',*,*,#3192,.F.);
#4349=ORIENTED_EDGE('',*,*,#3193,.T.);
#4350=ORIENTED_EDGE('',*,*,#3194,.T.);
#4351=ORIENTED_EDGE('',*,*,#3195,.T.);
#4352=ORIENTED_EDGE('',*,*,#3190,.F.);
#4353=ORIENTED_EDGE('',*,*,#3196,.T.);
#4354=ORIENTED_EDGE('',*,*,#3197,.T.);
#4355=ORIENTED_EDGE('',*,*,#3198,.T.);
#4356=ORIENTED_EDGE('',*,*,#3194,.F.);
#4357=ORIENTED_EDGE('',*,*,#3199,.T.);
#4358=ORIENTED_EDGE('',*,*,#3200,.T.);
#4359=ORIENTED_EDGE('',*,*,#3201,.T.);
#4360=ORIENTED_EDGE('',*,*,#3197,.F.);
#4361=ORIENTED_EDGE('',*,*,#3202,.T.);
#4362=ORIENTED_EDGE('',*,*,#3203,.T.);
#4363=ORIENTED_EDGE('',*,*,#3204,.T.);
#4364=ORIENTED_EDGE('',*,*,#3200,.F.);
#4365=ORIENTED_EDGE('',*,*,#3205,.T.);
#4366=ORIENTED_EDGE('',*,*,#3192,.T.);
#4367=ORIENTED_EDGE('',*,*,#3206,.T.);
#4368=ORIENTED_EDGE('',*,*,#3203,.F.);
#4369=ORIENTED_EDGE('',*,*,#3205,.F.);
#4370=ORIENTED_EDGE('',*,*,#3202,.F.);
#4371=ORIENTED_EDGE('',*,*,#3199,.F.);
#4372=ORIENTED_EDGE('',*,*,#3196,.F.);
#4373=ORIENTED_EDGE('',*,*,#3193,.F.);
#4374=ORIENTED_EDGE('',*,*,#3189,.F.);
#4375=ORIENTED_EDGE('',*,*,#3206,.F.);
#4376=ORIENTED_EDGE('',*,*,#3191,.F.);
#4377=ORIENTED_EDGE('',*,*,#3195,.F.);
#4378=ORIENTED_EDGE('',*,*,#3198,.F.);
#4379=ORIENTED_EDGE('',*,*,#3201,.F.);
#4380=ORIENTED_EDGE('',*,*,#3204,.F.);
#4466=CYLINDRICAL_SURFACE('',#5721,0.35);
#4467=CYLINDRICAL_SURFACE('',#5729,0.1954);
#4736=ADVANCED_FACE('',(#931),#652,.T.);
#4737=ADVANCED_FACE('',(#932),#211,.T.);
#4738=ADVANCED_FACE('',(#933),#4466,.T.);
#4739=ADVANCED_FACE('',(#934),#212,.T.);
#4740=ADVANCED_FACE('',(#935,#499),#653,.T.);
#4741=ADVANCED_FACE('',(#936),#213,.T.);
#4742=ADVANCED_FACE('',(#937),#4467,.T.);
#4743=ADVANCED_FACE('',(#938),#214,.T.);
#4744=ADVANCED_FACE('',(#939),#654,.T.);
#4745=ADVANCED_FACE('',(#940),#655,.F.);
#4746=ADVANCED_FACE('',(#941),#656,.F.);
#4747=ADVANCED_FACE('',(#942),#657,.F.);
#4748=ADVANCED_FACE('',(#943),#658,.F.);
#4749=ADVANCED_FACE('',(#944),#659,.F.);
#4750=ADVANCED_FACE('',(#945),#660,.F.);
#4751=ADVANCED_FACE('',(#946),#661,.F.);
#4752=ADVANCED_FACE('',(#947),#662,.F.);
#4794=CLOSED_SHELL('',(#4736,#4737,#4738,#4739,#4740,#4741,#4742,#4743,
#4744));
#4795=CLOSED_SHELL('',(#4745,#4746,#4747,#4748,#4749,#4750,#4751,#4752));
#5716=AXIS2_PLACEMENT_3D('',#9663,#7203,#7204);
#5717=AXIS2_PLACEMENT_3D('',#9664,#7205,#7206);
#5718=AXIS2_PLACEMENT_3D('',#9666,#7207,#7208);
#5719=AXIS2_PLACEMENT_3D('',#9667,#7209,#7210);
#5720=AXIS2_PLACEMENT_3D('',#9669,#7211,#7212);
#5721=AXIS2_PLACEMENT_3D('',#9671,#7214,#7215);
#5722=AXIS2_PLACEMENT_3D('',#9673,#7216,#7217);
#5723=AXIS2_PLACEMENT_3D('',#9675,#7219,#7220);
#5724=AXIS2_PLACEMENT_3D('',#9677,#7221,#7222);
#5725=AXIS2_PLACEMENT_3D('',#9679,#7224,#7225);
#5726=AXIS2_PLACEMENT_3D('',#9681,#7226,#7227);
#5727=AXIS2_PLACEMENT_3D('',#9682,#7228,#7229);
#5728=AXIS2_PLACEMENT_3D('',#9684,#7230,#7231);
#5729=AXIS2_PLACEMENT_3D('',#9686,#7233,#7234);
#5730=AXIS2_PLACEMENT_3D('',#9688,#7235,#7236);
#5731=AXIS2_PLACEMENT_3D('',#9690,#7238,#7239);
#5732=AXIS2_PLACEMENT_3D('',#9692,#7240,#7241);
#5733=AXIS2_PLACEMENT_3D('',#9694,#7243,#7244);
#5734=AXIS2_PLACEMENT_3D('',#9695,#7245,#7246);
#5735=AXIS2_PLACEMENT_3D('',#9704,#7251,#7252);
#5736=AXIS2_PLACEMENT_3D('',#9710,#7256,#7257);
#5737=AXIS2_PLACEMENT_3D('',#9716,#7261,#7262);
#5738=AXIS2_PLACEMENT_3D('',#9722,#7266,#7267);
#5739=AXIS2_PLACEMENT_3D('',#9728,#7271,#7272);
#5740=AXIS2_PLACEMENT_3D('',#9731,#7275,#7276);
#5741=AXIS2_PLACEMENT_3D('',#9732,#7277,#7278);
#7203=DIRECTION('axis',(0.,0.,1.));
#7204=DIRECTION('refdir',(1.,0.,0.));
#7205=DIRECTION('center_axis',(0.,1.,0.));
#7206=DIRECTION('ref_axis',(0.,0.,1.));
#7207=DIRECTION('center_axis',(0.,-1.,0.));
#7208=DIRECTION('ref_axis',(1.,0.,0.));
#7209=DIRECTION('center_axis',(0.,-1.,0.));
#7210=DIRECTION('ref_axis',(1.,0.,0.));
#7211=DIRECTION('center_axis',(0.,-1.,0.));
#7212=DIRECTION('ref_axis',(1.,0.,0.));
#7213=DIRECTION('',(0.707106781186547,0.707106781186548,8.65956056235493E-17));
#7214=DIRECTION('center_axis',(0.,-1.,0.));
#7215=DIRECTION('ref_axis',(1.,0.,0.));
#7216=DIRECTION('center_axis',(0.,-1.,0.));
#7217=DIRECTION('ref_axis',(1.,0.,0.));
#7218=DIRECTION('',(0.,1.,0.));
#7219=DIRECTION('center_axis',(0.,1.,0.));
#7220=DIRECTION('ref_axis',(1.,0.,0.));
#7221=DIRECTION('center_axis',(0.,-1.,0.));
#7222=DIRECTION('ref_axis',(1.,0.,0.));
#7223=DIRECTION('',(-0.707106781186547,0.707106781186548,-8.65956056235493E-17));
#7224=DIRECTION('center_axis',(0.,-1.,0.));
#7225=DIRECTION('ref_axis',(0.,0.,-1.));
#7226=DIRECTION('center_axis',(0.,-1.,0.));
#7227=DIRECTION('ref_axis',(1.,0.,0.));
#7228=DIRECTION('center_axis',(0.,1.,0.));
#7229=DIRECTION('ref_axis',(1.,0.,0.));
#7230=DIRECTION('center_axis',(0.,1.,0.));
#7231=DIRECTION('ref_axis',(1.,0.,0.));
#7232=DIRECTION('',(-0.447213595499958,0.894427190999916,-5.47678698264203E-17));
#7233=DIRECTION('center_axis',(0.,-1.,0.));
#7234=DIRECTION('ref_axis',(1.,0.,0.));
#7235=DIRECTION('center_axis',(0.,1.,0.));
#7236=DIRECTION('ref_axis',(1.,0.,0.));
#7237=DIRECTION('',(0.,1.,0.));
#7238=DIRECTION('center_axis',(0.,1.,0.));
#7239=DIRECTION('ref_axis',(1.,0.,0.));
#7240=DIRECTION('center_axis',(0.,-1.,0.));
#7241=DIRECTION('ref_axis',(1.,0.,0.));
#7242=DIRECTION('',(-0.707106781186547,0.707106781186548,-8.65956056235493E-17));
#7243=DIRECTION('center_axis',(0.,-1.,0.));
#7244=DIRECTION('ref_axis',(0.,0.,-1.));
#7245=DIRECTION('center_axis',(0.866025403784439,0.,-0.5));
#7246=DIRECTION('ref_axis',(0.5,0.,0.866025403784439));
#7247=DIRECTION('',(-0.5,0.,-0.866025403784439));
#7248=DIRECTION('',(0.,-1.,0.));
#7249=DIRECTION('',(0.5,0.,0.866025403784439));
#7250=DIRECTION('',(0.,-1.,0.));
#7251=DIRECTION('center_axis',(1.60246890531964E-16,0.,-1.));
#7252=DIRECTION('ref_axis',(1.,0.,1.60246890531964E-16));
#7253=DIRECTION('',(-1.,0.,-1.60246890531964E-16));
#7254=DIRECTION('',(0.,-1.,0.));
#7255=DIRECTION('',(1.,0.,1.60246890531964E-16));
#7256=DIRECTION('center_axis',(-0.866025403784439,0.,-0.5));
#7257=DIRECTION('ref_axis',(0.5,0.,-0.866025403784439));
#7258=DIRECTION('',(-0.5,0.,0.866025403784439));
#7259=DIRECTION('',(0.,-1.,0.));
#7260=DIRECTION('',(0.5,0.,-0.866025403784439));
#7261=DIRECTION('center_axis',(-0.866025403784439,0.,0.5));
#7262=DIRECTION('ref_axis',(-0.5,0.,-0.866025403784439));
#7263=DIRECTION('',(0.5,0.,0.866025403784439));
#7264=DIRECTION('',(0.,-1.,0.));
#7265=DIRECTION('',(-0.5,0.,-0.866025403784439));
#7266=DIRECTION('center_axis',(-1.60246890531964E-16,0.,1.));
#7267=DIRECTION('ref_axis',(-1.,0.,-1.60246890531964E-16));
#7268=DIRECTION('',(1.,0.,1.60246890531964E-16));
#7269=DIRECTION('',(0.,-1.,0.));
#7270=DIRECTION('',(-1.,0.,-1.60246890531964E-16));
#7271=DIRECTION('center_axis',(0.866025403784439,0.,0.5));
#7272=DIRECTION('ref_axis',(-0.5,0.,0.866025403784439));
#7273=DIRECTION('',(0.5,0.,-0.866025403784439));
#7274=DIRECTION('',(-0.5,0.,0.866025403784439));
#7275=DIRECTION('center_axis',(0.,1.,0.));
#7276=DIRECTION('ref_axis',(1.,0.,0.));
#7277=DIRECTION('center_axis',(0.,-1.,0.));
#7278=DIRECTION('ref_axis',(0.,0.,-1.));
#9663=CARTESIAN_POINT('',(0.,0.,0.));
#9664=CARTESIAN_POINT('Origin',(0.3,0.4,0.));
#9665=CARTESIAN_POINT('',(-0.3,0.4,-3.67394039744206E-17));
#9666=CARTESIAN_POINT('Origin',(0.,0.4,0.));
#9667=CARTESIAN_POINT('Origin',(0.,0.375,0.));
#9668=CARTESIAN_POINT('',(-0.35,0.35,-4.28626379701573E-17));
#9669=CARTESIAN_POINT('Origin',(0.,0.35,0.));
#9670=CARTESIAN_POINT('',(-0.325,0.375,-3.9801020972289E-17));
#9671=CARTESIAN_POINT('Origin',(0.,0.19,0.));
#9672=CARTESIAN_POINT('',(-0.35,0.03,-4.28626379701574E-17));
#9673=CARTESIAN_POINT('Origin',(0.,0.03,0.));
#9674=CARTESIAN_POINT('',(-0.35,0.19,-4.28626379701574E-17));
#9675=CARTESIAN_POINT('Origin',(0.,0.0149999999999999,0.));
#9676=CARTESIAN_POINT('',(-0.32,-3.29597460435593E-17,-3.91886975727153E-17));
#9677=CARTESIAN_POINT('Origin',(0.,0.,0.));
#9678=CARTESIAN_POINT('',(-0.335,0.0149999999999999,-4.10256677714363E-17));
#9679=CARTESIAN_POINT('Origin',(0.22,0.,0.));
#9680=CARTESIAN_POINT('',(-0.22,-6.93889390390723E-18,-2.69422295812418E-17));
#9681=CARTESIAN_POINT('Origin',(0.,0.,0.));
#9682=CARTESIAN_POINT('Origin',(0.,-0.02,0.));
#9683=CARTESIAN_POINT('',(-0.1954,-0.0492,2.39295984553393E-17));
#9684=CARTESIAN_POINT('Origin',(0.,-0.0492,0.));
#9685=CARTESIAN_POINT('',(-0.21,-0.02,-2.57175827820944E-17));
#9686=CARTESIAN_POINT('Origin',(0.,-0.8,0.));
#9687=CARTESIAN_POINT('',(-0.1954,-1.5646,2.39295984553393E-17));
#9688=CARTESIAN_POINT('Origin',(0.,-1.5646,0.));
#9689=CARTESIAN_POINT('',(-0.1954,-0.8,-2.39295984553393E-17));
#9690=CARTESIAN_POINT('Origin',(0.,-1.58,0.));
#9691=CARTESIAN_POINT('',(-0.16,-1.6,-1.95943487863577E-17));
#9692=CARTESIAN_POINT('Origin',(0.,-1.6,0.));
#9693=CARTESIAN_POINT('',(-0.18,-1.58,-2.20436423846524E-17));
#9694=CARTESIAN_POINT('Origin',(0.,-1.6,0.));
#9695=CARTESIAN_POINT('Origin',(0.0866025403784439,-0.4,-0.15));
#9696=CARTESIAN_POINT('',(0.173205080756888,-0.4,0.));
#9697=CARTESIAN_POINT('',(0.0866025403784439,-0.4,-0.15));
#9698=CARTESIAN_POINT('',(0.173205080756888,-0.4,0.));
#9699=CARTESIAN_POINT('',(0.0866025403784439,-0.64,-0.15));
#9700=CARTESIAN_POINT('',(0.0866025403784439,-0.4,-0.15));
#9701=CARTESIAN_POINT('',(0.173205080756888,-0.64,0.));
#9702=CARTESIAN_POINT('',(0.173205080756888,-0.64,0.));
#9703=CARTESIAN_POINT('',(0.173205080756888,-0.4,0.));
#9704=CARTESIAN_POINT('Origin',(-0.0866025403784438,-0.4,-0.15));
#9705=CARTESIAN_POINT('',(-0.0866025403784438,-0.4,-0.15));
#9706=CARTESIAN_POINT('',(0.0866025403784439,-0.4,-0.15));
#9707=CARTESIAN_POINT('',(-0.0866025403784438,-0.64,-0.15));
#9708=CARTESIAN_POINT('',(-0.0866025403784438,-0.4,-0.15));
#9709=CARTESIAN_POINT('',(0.0866025403784439,-0.64,-0.15));
#9710=CARTESIAN_POINT('Origin',(-0.173205080756888,-0.4,-2.77555756156289E-17));
#9711=CARTESIAN_POINT('',(-0.173205080756888,-0.4,-2.12115047744981E-17));
#9712=CARTESIAN_POINT('',(-0.0866025403784438,-0.4,-0.15));
#9713=CARTESIAN_POINT('',(-0.173205080756888,-0.64,-2.77555756156289E-17));
#9714=CARTESIAN_POINT('',(-0.173205080756888,-0.4,-2.12115047744981E-17));
#9715=CARTESIAN_POINT('',(-0.0866025403784438,-0.64,-0.15));
#9716=CARTESIAN_POINT('Origin',(-0.0866025403784439,-0.4,0.15));
#9717=CARTESIAN_POINT('',(-0.0866025403784439,-0.4,0.15));
#9718=CARTESIAN_POINT('',(-0.173205080756888,-0.4,-2.12115047744981E-17));
#9719=CARTESIAN_POINT('',(-0.0866025403784439,-0.64,0.15));
#9720=CARTESIAN_POINT('',(-0.0866025403784439,-0.4,0.15));
#9721=CARTESIAN_POINT('',(-0.173205080756888,-0.64,-2.12115047744981E-17));
#9722=CARTESIAN_POINT('Origin',(0.0866025403784439,-0.4,0.15));
#9723=CARTESIAN_POINT('',(0.0866025403784439,-0.4,0.15));
#9724=CARTESIAN_POINT('',(-0.0866025403784439,-0.4,0.15));
#9725=CARTESIAN_POINT('',(0.0866025403784439,-0.64,0.15));
#9726=CARTESIAN_POINT('',(0.0866025403784439,-0.4,0.15));
#9727=CARTESIAN_POINT('',(-0.0866025403784439,-0.64,0.15));
#9728=CARTESIAN_POINT('Origin',(0.173205080756888,-0.4,0.));
#9729=CARTESIAN_POINT('',(0.0866025403784439,-0.4,0.15));
#9730=CARTESIAN_POINT('',(0.0866025403784439,-0.64,0.15));
#9731=CARTESIAN_POINT('Origin',(0.,-0.4,-2.77555756156289E-17));
#9732=CARTESIAN_POINT('Origin',(0.,-0.64,-2.77555756156289E-17));
#9776=UNCERTAINTY_MEASURE_WITH_UNIT(LENGTH_MEASURE(0.001),#9814,
'DISTANCE_ACCURACY_VALUE',
'Maximum model space distance between geometric entities at asserted c
onnectivities');
#9777=UNCERTAINTY_MEASURE_WITH_UNIT(LENGTH_MEASURE(0.001),#9814,
'DISTANCE_ACCURACY_VALUE',
'Maximum model space distance between geometric entities at asserted c
onnectivities');
#9812=(
GEOMETRIC_REPRESENTATION_CONTEXT(3)
GLOBAL_UNCERTAINTY_ASSIGNED_CONTEXT((#9776))
GLOBAL_UNIT_ASSIGNED_CONTEXT((#9814,#9816,#9817))
REPRESENTATION_CONTEXT('','3D')
);
#9813=(
GEOMETRIC_REPRESENTATION_CONTEXT(3)
GLOBAL_UNCERTAINTY_ASSIGNED_CONTEXT((#9777))
GLOBAL_UNIT_ASSIGNED_CONTEXT((#9814,#9816,#9817))
REPRESENTATION_CONTEXT('','3D')
);
#9814=(
LENGTH_UNIT()
NAMED_UNIT(*)
SI_UNIT(.CENTI.,.METRE.)
);
#9816=(
NAMED_UNIT(*)
PLANE_ANGLE_UNIT()
SI_UNIT($,.RADIAN.)
);
#9817=(
NAMED_UNIT(*)
SI_UNIT($,.STERADIAN.)
SOLID_ANGLE_UNIT()
);
#9852=SHAPE_DEFINITION_REPRESENTATION(#9925,#9969);
#9925=PRODUCT_DEFINITION_SHAPE('',$,#10005);
#9969=SHAPE_REPRESENTATION('',(#5716),#9812);
#9970=PRODUCT_DEFINITION_CONTEXT('part definition',#10077,'design');
#10005=PRODUCT_DEFINITION('Cap Screw - M4x16','Cap Screw - M4x16',#10040,
#9970);
#10040=PRODUCT_DEFINITION_FORMATION('',$,#10113);
#10077=APPLICATION_CONTEXT(
'Core Data for Automotive Mechanical Design Process');
#10078=PRODUCT_CONTEXT('part definition',#10077,'mechanical');
#10113=PRODUCT('Cap Screw - M4x16','Cap Screw - M4x16',
'Cap Screw - M4x16',(#10078));
#10184=COLOUR_RGB('Black',0.12,0.14,0.17);
#10185=FILL_AREA_STYLE_COLOUR('',#10184);
#10186=FILL_AREA_STYLE('',(#10185));
#10187=SURFACE_STYLE_FILL_AREA(#10186);
#10188=SURFACE_SIDE_STYLE('',(#10187));
#10189=SURFACE_STYLE_USAGE(.BOTH.,#10188);
#10190=PRESENTATION_STYLE_ASSIGNMENT((#10189));
ENDSEC;
END-ISO-10303-21;
